ISO-10303-21;
HEADER;
/* Generated by software containing ST-Developer
 * from STEP Tools, Inc. (www.steptools.com) 
 */

FILE_DESCRIPTION(
/* description */ ('Bearing-mounted hook block'),
/* implementation_level */ '2;1');

FILE_NAME(
/* name */ 'M8x75 cross bolt.step',
/* time_stamp */ '2026-10-28T22:30:11-07:00',
/* author */ (''),
/* organization */ (''),
/* preprocessor_version */ 'ST-DEVELOPER v20.2',
/* originating_system */ 'Autodesk Translation Framework v15.17.0.0',
/* authorisation */ '');

FILE_SCHEMA (('AUTOMOTIVE_DESIGN { 1 0 10303 214 3 1 1 }'));
ENDSEC;

DATA;
#10=MECHANICAL_DESIGN_GEOMETRIC_PRESENTATION_REPRESENTATION('',(#331),#7609);
#251=CONICAL_SURFACE('',#4373,0.625,0.785398163397448);
#252=CONICAL_SURFACE('',#4377,0.635,0.785398163397449);
#253=CONICAL_SURFACE('',#4381,0.41,0.463647609000806);
#269=ORIENTED_CLOSED_SHELL('',*,#3927,.F.);
#272=BREP_WITH_VOIDS('Body1',#3928,(#269));
#283=SHAPE_REPRESENTATION_RELATIONSHIP('SRR','None',#7730,#307);
#307=ADVANCED_BREP_SHAPE_REPRESENTATION('',(#272),#7590);
#331=STYLED_ITEM('',(#7938),#272);
#453=LINE('',#6363,#683);
#454=LINE('',#6365,#684);
#455=LINE('',#6367,#685);
#456=LINE('',#6368,#686);
#457=LINE('',#6371,#687);
#458=LINE('',#6373,#688);
#459=LINE('',#6374,#689);
#460=LINE('',#6377,#690);
#461=LINE('',#6379,#691);
#462=LINE('',#6380,#692);
#463=LINE('',#6383,#693);
#464=LINE('',#6385,#694);
#465=LINE('',#6386,#695);
#466=LINE('',#6389,#696);
#467=LINE('',#6391,#697);
#468=LINE('',#6392,#698);
#469=LINE('',#6394,#699);
#470=LINE('',#6395,#700);
#471=LINE('',#6405,#701);
#472=LINE('',#6414,#702);
#473=LINE('',#6418,#703);
#474=LINE('',#6422,#704);
#475=LINE('',#6429,#705);
#476=LINE('',#6431,#706);
#683=VECTOR('',#5104,1.);
#684=VECTOR('',#5105,1.);
#685=VECTOR('',#5106,1.);
#686=VECTOR('',#5107,1.);
#687=VECTOR('',#5110,1.);
#688=VECTOR('',#5111,1.);
#689=VECTOR('',#5112,1.);
#690=VECTOR('',#5115,1.);
#691=VECTOR('',#5116,1.);
#692=VECTOR('',#5117,1.);
#693=VECTOR('',#5120,1.);
#694=VECTOR('',#5121,1.);
#695=VECTOR('',#5122,1.);
#696=VECTOR('',#5125,1.);
#697=VECTOR('',#5126,1.);
#698=VECTOR('',#5127,1.);
#699=VECTOR('',#5130,1.);
#700=VECTOR('',#5131,1.);
#701=VECTOR('',#5144,0.4);
#702=VECTOR('',#5157,0.625);
#703=VECTOR('',#5162,0.65);
#704=VECTOR('',#5167,0.635);
#705=VECTOR('',#5176,0.41);
#706=VECTOR('',#5179,0.4);
#873=CYLINDRICAL_SURFACE('',#4368,0.4);
#874=CYLINDRICAL_SURFACE('',#4375,0.65);
#875=CYLINDRICAL_SURFACE('',#4383,0.3933);
#953=FACE_BOUND('',#1339,.T.);
#954=FACE_BOUND('',#1347,.T.);
#1062=FACE_OUTER_BOUND('',#1330,.T.);
#1063=FACE_OUTER_BOUND('',#1331,.T.);
#1064=FACE_OUTER_BOUND('',#1332,.T.);
#1065=FACE_OUTER_BOUND('',#1333,.T.);
#1066=FACE_OUTER_BOUND('',#1334,.T.);
#1067=FACE_OUTER_BOUND('',#1335,.T.);
#1068=FACE_OUTER_BOUND('',#1336,.T.);
#1069=FACE_OUTER_BOUND('',#1337,.T.);
#1070=FACE_OUTER_BOUND('',#1338,.T.);
#1071=FACE_OUTER_BOUND('',#1340,.T.);
#1072=FACE_OUTER_BOUND('',#1341,.T.);
#1073=FACE_OUTER_BOUND('',#1342,.T.);
#1074=FACE_OUTER_BOUND('',#1343,.T.);
#1075=FACE_OUTER_BOUND('',#1344,.T.);
#1076=FACE_OUTER_BOUND('',#1345,.T.);
#1077=FACE_OUTER_BOUND('',#1346,.T.);
#1078=FACE_OUTER_BOUND('',#1348,.T.);
#1079=FACE_OUTER_BOUND('',#1349,.T.);
#1330=EDGE_LOOP('',(#2860,#2861,#2862,#2863));
#1331=EDGE_LOOP('',(#2864,#2865,#2866,#2867));
#1332=EDGE_LOOP('',(#2868,#2869,#2870,#2871));
#1333=EDGE_LOOP('',(#2872,#2873,#2874,#2875));
#1334=EDGE_LOOP('',(#2876,#2877,#2878,#2879));
#1335=EDGE_LOOP('',(#2880,#2881,#2882,#2883));
#1336=EDGE_LOOP('',(#2884,#2885,#2886,#2887,#2888,#2889));
#1337=EDGE_LOOP('',(#2890,#2891,#2892,#2893,#2894,#2895));
#1338=EDGE_LOOP('',(#2896));
#1339=EDGE_LOOP('',(#2897));
#1340=EDGE_LOOP('',(#2898,#2899,#2900,#2901));
#1341=EDGE_LOOP('',(#2902));
#1342=EDGE_LOOP('',(#2903));
#1343=EDGE_LOOP('',(#2904,#2905,#2906,#2907));
#1344=EDGE_LOOP('',(#2908,#2909,#2910,#2911));
#1345=EDGE_LOOP('',(#2912,#2913,#2914,#2915));
#1346=EDGE_LOOP('',(#2916));
#1347=EDGE_LOOP('',(#2917));
#1348=EDGE_LOOP('',(#2918,#2919,#2920,#2921));
#1349=EDGE_LOOP('',(#2922,#2923,#2924,#2925));
#1619=CIRCLE('',#4366,0.4);
#1620=CIRCLE('',#4367,0.3933);
#1621=CIRCLE('',#4369,0.4);
#1622=CIRCLE('',#4372,0.6);
#1623=CIRCLE('',#4374,0.65);
#1624=CIRCLE('',#4376,0.65);
#1625=CIRCLE('',#4378,0.62);
#1626=CIRCLE('',#4380,0.42);
#1627=CIRCLE('',#4382,0.3933);
#1868=VERTEX_POINT('',#6361);
#1869=VERTEX_POINT('',#6362);
#1870=VERTEX_POINT('',#6364);
#1871=VERTEX_POINT('',#6366);
#1872=VERTEX_POINT('',#6370);
#1873=VERTEX_POINT('',#6372);
#1874=VERTEX_POINT('',#6376);
#1875=VERTEX_POINT('',#6378);
#1876=VERTEX_POINT('',#6382);
#1877=VERTEX_POINT('',#6384);
#1878=VERTEX_POINT('',#6388);
#1879=VERTEX_POINT('',#6390);
#1880=VERTEX_POINT('',#6399);
#1881=VERTEX_POINT('',#6401);
#1882=VERTEX_POINT('',#6404);
#1883=VERTEX_POINT('',#6409);
#1884=VERTEX_POINT('',#6412);
#1885=VERTEX_POINT('',#6416);
#1886=VERTEX_POINT('',#6420);
#1887=VERTEX_POINT('',#6424);
#1888=VERTEX_POINT('',#6427);
#2240=EDGE_CURVE('',#1868,#1869,#453,.T.);
#2241=EDGE_CURVE('',#1869,#1870,#454,.T.);
#2242=EDGE_CURVE('',#1870,#1871,#455,.T.);
#2243=EDGE_CURVE('',#1868,#1871,#456,.T.);
#2244=EDGE_CURVE('',#1869,#1872,#457,.T.);
#2245=EDGE_CURVE('',#1872,#1873,#458,.T.);
#2246=EDGE_CURVE('',#1873,#1870,#459,.T.);
#2247=EDGE_CURVE('',#1872,#1874,#460,.T.);
#2248=EDGE_CURVE('',#1874,#1875,#461,.T.);
#2249=EDGE_CURVE('',#1875,#1873,#462,.T.);
#2250=EDGE_CURVE('',#1874,#1876,#463,.T.);
#2251=EDGE_CURVE('',#1876,#1877,#464,.T.);
#2252=EDGE_CURVE('',#1877,#1875,#465,.T.);
#2253=EDGE_CURVE('',#1876,#1878,#466,.T.);
#2254=EDGE_CURVE('',#1878,#1879,#467,.T.);
#2255=EDGE_CURVE('',#1879,#1877,#468,.T.);
#2256=EDGE_CURVE('',#1878,#1868,#469,.T.);
#2257=EDGE_CURVE('',#1871,#1879,#470,.T.);
#2258=EDGE_CURVE('',#1880,#1880,#1619,.T.);
#2259=EDGE_CURVE('',#1881,#1881,#1620,.T.);
#2260=EDGE_CURVE('',#1880,#1882,#471,.T.);
#2261=EDGE_CURVE('',#1882,#1882,#1621,.T.);
#2262=EDGE_CURVE('',#1883,#1883,#1622,.T.);
#2263=EDGE_CURVE('',#1884,#1884,#1623,.T.);
#2264=EDGE_CURVE('',#1884,#1883,#472,.T.);
#2265=EDGE_CURVE('',#1885,#1885,#1624,.T.);
#2266=EDGE_CURVE('',#1885,#1884,#473,.T.);
#2267=EDGE_CURVE('',#1886,#1886,#1625,.T.);
#2268=EDGE_CURVE('',#1886,#1885,#474,.T.);
#2269=EDGE_CURVE('',#1887,#1887,#1626,.T.);
#2270=EDGE_CURVE('',#1888,#1888,#1627,.F.);
#2271=EDGE_CURVE('',#1888,#1887,#475,.T.);
#2272=EDGE_CURVE('',#1881,#1888,#476,.T.);
#2860=ORIENTED_EDGE('',*,*,#2240,.T.);
#2861=ORIENTED_EDGE('',*,*,#2241,.T.);
#2862=ORIENTED_EDGE('',*,*,#2242,.T.);
#2863=ORIENTED_EDGE('',*,*,#2243,.F.);
#2864=ORIENTED_EDGE('',*,*,#2244,.T.);
#2865=ORIENTED_EDGE('',*,*,#2245,.T.);
#2866=ORIENTED_EDGE('',*,*,#2246,.T.);
#2867=ORIENTED_EDGE('',*,*,#2241,.F.);
#2868=ORIENTED_EDGE('',*,*,#2247,.T.);
#2869=ORIENTED_EDGE('',*,*,#2248,.T.);
#2870=ORIENTED_EDGE('',*,*,#2249,.T.);
#2871=ORIENTED_EDGE('',*,*,#2245,.F.);
#2872=ORIENTED_EDGE('',*,*,#2250,.T.);
#2873=ORIENTED_EDGE('',*,*,#2251,.T.);
#2874=ORIENTED_EDGE('',*,*,#2252,.T.);
#2875=ORIENTED_EDGE('',*,*,#2248,.F.);
#2876=ORIENTED_EDGE('',*,*,#2253,.T.);
#2877=ORIENTED_EDGE('',*,*,#2254,.T.);
#2878=ORIENTED_EDGE('',*,*,#2255,.T.);
#2879=ORIENTED_EDGE('',*,*,#2251,.F.);
#2880=ORIENTED_EDGE('',*,*,#2256,.T.);
#2881=ORIENTED_EDGE('',*,*,#2243,.T.);
#2882=ORIENTED_EDGE('',*,*,#2257,.T.);
#2883=ORIENTED_EDGE('',*,*,#2254,.F.);
#2884=ORIENTED_EDGE('',*,*,#2256,.F.);
#2885=ORIENTED_EDGE('',*,*,#2253,.F.);
#2886=ORIENTED_EDGE('',*,*,#2250,.F.);
#2887=ORIENTED_EDGE('',*,*,#2247,.F.);
#2888=ORIENTED_EDGE('',*,*,#2244,.F.);
#2889=ORIENTED_EDGE('',*,*,#2240,.F.);
#2890=ORIENTED_EDGE('',*,*,#2257,.F.);
#2891=ORIENTED_EDGE('',*,*,#2242,.F.);
#2892=ORIENTED_EDGE('',*,*,#2246,.F.);
#2893=ORIENTED_EDGE('',*,*,#2249,.F.);
#2894=ORIENTED_EDGE('',*,*,#2252,.F.);
#2895=ORIENTED_EDGE('',*,*,#2255,.F.);
#2896=ORIENTED_EDGE('',*,*,#2258,.T.);
#2897=ORIENTED_EDGE('',*,*,#2259,.F.);
#2898=ORIENTED_EDGE('',*,*,#2258,.F.);
#2899=ORIENTED_EDGE('',*,*,#2260,.T.);
#2900=ORIENTED_EDGE('',*,*,#2261,.T.);
#2901=ORIENTED_EDGE('',*,*,#2260,.F.);
#2902=ORIENTED_EDGE('',*,*,#2261,.F.);
#2903=ORIENTED_EDGE('',*,*,#2262,.F.);
#2904=ORIENTED_EDGE('',*,*,#2263,.F.);
#2905=ORIENTED_EDGE('',*,*,#2264,.T.);
#2906=ORIENTED_EDGE('',*,*,#2262,.T.);
#2907=ORIENTED_EDGE('',*,*,#2264,.F.);
#2908=ORIENTED_EDGE('',*,*,#2265,.F.);
#2909=ORIENTED_EDGE('',*,*,#2266,.T.);
#2910=ORIENTED_EDGE('',*,*,#2263,.T.);
#2911=ORIENTED_EDGE('',*,*,#2266,.F.);
#2912=ORIENTED_EDGE('',*,*,#2267,.F.);
#2913=ORIENTED_EDGE('',*,*,#2268,.T.);
#2914=ORIENTED_EDGE('',*,*,#2265,.T.);
#2915=ORIENTED_EDGE('',*,*,#2268,.F.);
#2916=ORIENTED_EDGE('',*,*,#2267,.T.);
#2917=ORIENTED_EDGE('',*,*,#2269,.F.);
#2918=ORIENTED_EDGE('',*,*,#2270,.F.);
#2919=ORIENTED_EDGE('',*,*,#2271,.T.);
#2920=ORIENTED_EDGE('',*,*,#2269,.T.);
#2921=ORIENTED_EDGE('',*,*,#2271,.F.);
#2922=ORIENTED_EDGE('',*,*,#2259,.T.);
#2923=ORIENTED_EDGE('',*,*,#2272,.T.);
#2924=ORIENTED_EDGE('',*,*,#2270,.T.);
#2925=ORIENTED_EDGE('',*,*,#2272,.F.);
#3592=PLANE('',#4357);
#3593=PLANE('',#4358);
#3594=PLANE('',#4359);
#3595=PLANE('',#4360);
#3596=PLANE('',#4361);
#3597=PLANE('',#4362);
#3598=PLANE('',#4363);
#3599=PLANE('',#4364);
#3600=PLANE('',#4365);
#3601=PLANE('',#4370);
#3602=PLANE('',#4371);
#3603=PLANE('',#4379);
#3744=ADVANCED_FACE('',(#1062),#3592,.F.);
#3745=ADVANCED_FACE('',(#1063),#3593,.F.);
#3746=ADVANCED_FACE('',(#1064),#3594,.F.);
#3747=ADVANCED_FACE('',(#1065),#3595,.F.);
#3748=ADVANCED_FACE('',(#1066),#3596,.F.);
#3749=ADVANCED_FACE('',(#1067),#3597,.F.);
#3750=ADVANCED_FACE('',(#1068),#3598,.F.);
#3751=ADVANCED_FACE('',(#1069),#3599,.F.);
#3752=ADVANCED_FACE('',(#1070,#953),#3600,.T.);
#3753=ADVANCED_FACE('',(#1071),#873,.T.);
#3754=ADVANCED_FACE('',(#1072),#3601,.F.);
#3755=ADVANCED_FACE('',(#1073),#3602,.T.);
#3756=ADVANCED_FACE('',(#1074),#251,.T.);
#3757=ADVANCED_FACE('',(#1075),#874,.T.);
#3758=ADVANCED_FACE('',(#1076),#252,.T.);
#3759=ADVANCED_FACE('',(#1077,#954),#3603,.T.);
#3760=ADVANCED_FACE('',(#1078),#253,.T.);
#3761=ADVANCED_FACE('',(#1079),#875,.T.);
#3927=CLOSED_SHELL('',(#3744,#3745,#3746,#3747,#3748,#3749,#3750,#3751));
#3928=CLOSED_SHELL('',(#3752,#3753,#3754,#3755,#3756,#3757,#3758,#3759,
#3760,#3761));
#4356=AXIS2_PLACEMENT_3D('',#6359,#5100,#5101);
#4357=AXIS2_PLACEMENT_3D('',#6360,#5102,#5103);
#4358=AXIS2_PLACEMENT_3D('',#6369,#5108,#5109);
#4359=AXIS2_PLACEMENT_3D('',#6375,#5113,#5114);
#4360=AXIS2_PLACEMENT_3D('',#6381,#5118,#5119);
#4361=AXIS2_PLACEMENT_3D('',#6387,#5123,#5124);
#4362=AXIS2_PLACEMENT_3D('',#6393,#5128,#5129);
#4363=AXIS2_PLACEMENT_3D('',#6396,#5132,#5133);
#4364=AXIS2_PLACEMENT_3D('',#6397,#5134,#5135);
#4365=AXIS2_PLACEMENT_3D('',#6398,#5136,#5137);
#4366=AXIS2_PLACEMENT_3D('',#6400,#5138,#5139);
#4367=AXIS2_PLACEMENT_3D('',#6402,#5140,#5141);
#4368=AXIS2_PLACEMENT_3D('',#6403,#5142,#5143);
#4369=AXIS2_PLACEMENT_3D('',#6406,#5145,#5146);
#4370=AXIS2_PLACEMENT_3D('',#6407,#5147,#5148);
#4371=AXIS2_PLACEMENT_3D('',#6408,#5149,#5150);
#4372=AXIS2_PLACEMENT_3D('',#6410,#5151,#5152);
#4373=AXIS2_PLACEMENT_3D('',#6411,#5153,#5154);
#4374=AXIS2_PLACEMENT_3D('',#6413,#5155,#5156);
#4375=AXIS2_PLACEMENT_3D('',#6415,#5158,#5159);
#4376=AXIS2_PLACEMENT_3D('',#6417,#5160,#5161);
#4377=AXIS2_PLACEMENT_3D('',#6419,#5163,#5164);
#4378=AXIS2_PLACEMENT_3D('',#6421,#5165,#5166);
#4379=AXIS2_PLACEMENT_3D('',#6423,#5168,#5169);
#4380=AXIS2_PLACEMENT_3D('',#6425,#5170,#5171);
#4381=AXIS2_PLACEMENT_3D('',#6426,#5172,#5173);
#4382=AXIS2_PLACEMENT_3D('',#6428,#5174,#5175);
#4383=AXIS2_PLACEMENT_3D('',#6430,#5177,#5178);
#5100=DIRECTION('axis',(0.,0.,1.));
#5101=DIRECTION('refdir',(1.,0.,0.));
#5102=DIRECTION('center_axis',(0.866025403784439,0.,-0.5));
#5103=DIRECTION('ref_axis',(0.5,0.,0.866025403784439));
#5104=DIRECTION('',(-0.5,0.,-0.866025403784439));
#5105=DIRECTION('',(0.,-1.,0.));
#5106=DIRECTION('',(0.5,0.,0.866025403784439));
#5107=DIRECTION('',(0.,-1.,0.));
#5108=DIRECTION('center_axis',(1.60246890531964E-16,0.,-1.));
#5109=DIRECTION('ref_axis',(1.,0.,1.60246890531964E-16));
#5110=DIRECTION('',(-1.,0.,-1.60246890531964E-16));
#5111=DIRECTION('',(0.,-1.,0.));
#5112=DIRECTION('',(1.,0.,1.60246890531964E-16));
#5113=DIRECTION('center_axis',(-0.866025403784439,0.,-0.5));
#5114=DIRECTION('ref_axis',(0.5,0.,-0.866025403784439));
#5115=DIRECTION('',(-0.5,0.,0.866025403784439));
#5116=DIRECTION('',(0.,-1.,0.));
#5117=DIRECTION('',(0.5,0.,-0.866025403784439));
#5118=DIRECTION('center_axis',(-0.866025403784439,0.,0.5));
#5119=DIRECTION('ref_axis',(-0.5,0.,-0.866025403784439));
#5120=DIRECTION('',(0.5,0.,0.866025403784439));
#5121=DIRECTION('',(0.,-1.,0.));
#5122=DIRECTION('',(-0.5,0.,-0.866025403784439));
#5123=DIRECTION('center_axis',(-1.60246890531964E-16,0.,1.));
#5124=DIRECTION('ref_axis',(-1.,0.,-1.60246890531964E-16));
#5125=DIRECTION('',(1.,0.,1.60246890531964E-16));
#5126=DIRECTION('',(0.,-1.,0.));
#5127=DIRECTION('',(-1.,0.,-1.60246890531964E-16));
#5128=DIRECTION('center_axis',(0.866025403784439,0.,0.5));
#5129=DIRECTION('ref_axis',(-0.5,0.,0.866025403784439));
#5130=DIRECTION('',(0.5,0.,-0.866025403784439));
#5131=DIRECTION('',(-0.5,0.,0.866025403784439));
#5132=DIRECTION('center_axis',(0.,1.,0.));
#5133=DIRECTION('ref_axis',(1.,0.,0.));
#5134=DIRECTION('center_axis',(0.,-1.,0.));
#5135=DIRECTION('ref_axis',(0.,0.,-1.));
#5136=DIRECTION('center_axis',(0.,1.,0.));
#5137=DIRECTION('ref_axis',(1.,0.,0.));
#5138=DIRECTION('center_axis',(0.,1.,0.));
#5139=DIRECTION('ref_axis',(1.,0.,0.));
#5140=DIRECTION('center_axis',(0.,1.,0.));
#5141=DIRECTION('ref_axis',(1.,0.,0.));
#5142=DIRECTION('center_axis',(0.,1.,0.));
#5143=DIRECTION('ref_axis',(1.,0.,0.));
#5144=DIRECTION('',(0.,-1.,0.));
#5145=DIRECTION('center_axis',(0.,1.,0.));
#5146=DIRECTION('ref_axis',(1.,0.,0.));
#5147=DIRECTION('center_axis',(0.,1.,0.));
#5148=DIRECTION('ref_axis',(1.,0.,0.));
#5149=DIRECTION('center_axis',(0.,1.,0.));
#5150=DIRECTION('ref_axis',(0.,0.,1.));
#5151=DIRECTION('center_axis',(0.,-1.,0.));
#5152=DIRECTION('ref_axis',(1.,0.,0.));
#5153=DIRECTION('center_axis',(0.,-1.,0.));
#5154=DIRECTION('ref_axis',(1.,0.,0.));
#5155=DIRECTION('center_axis',(0.,-1.,0.));
#5156=DIRECTION('ref_axis',(1.,0.,0.));
#5157=DIRECTION('',(0.707106781186548,0.707106781186547,8.65956056235493E-17));
#5158=DIRECTION('center_axis',(0.,-1.,0.));
#5159=DIRECTION('ref_axis',(1.,0.,0.));
#5160=DIRECTION('center_axis',(0.,-1.,0.));
#5161=DIRECTION('ref_axis',(1.,0.,0.));
#5162=DIRECTION('',(0.,1.,0.));
#5163=DIRECTION('center_axis',(0.,1.,0.));
#5164=DIRECTION('ref_axis',(1.,0.,0.));
#5165=DIRECTION('center_axis',(0.,-1.,0.));
#5166=DIRECTION('ref_axis',(1.,0.,0.));
#5167=DIRECTION('',(-0.707106781186548,0.707106781186547,-8.65956056235494E-17));
#5168=DIRECTION('center_axis',(0.,-1.,0.));
#5169=DIRECTION('ref_axis',(0.,0.,-1.));
#5170=DIRECTION('center_axis',(0.,-1.,0.));
#5171=DIRECTION('ref_axis',(1.,0.,0.));
#5172=DIRECTION('center_axis',(0.,1.,0.));
#5173=DIRECTION('ref_axis',(1.,0.,0.));
#5174=DIRECTION('center_axis',(0.,1.,0.));
#5175=DIRECTION('ref_axis',(1.,0.,0.));
#5176=DIRECTION('',(-0.447213595499958,0.894427190999916,-5.47678698264203E-17));
#5177=DIRECTION('center_axis',(0.,-1.,0.));
#5178=DIRECTION('ref_axis',(1.,0.,0.));
#5179=DIRECTION('',(0.,1.,0.));
#6359=CARTESIAN_POINT('',(0.,0.,0.));
#6360=CARTESIAN_POINT('Origin',(0.173205080756888,-0.8,-0.3));
#6361=CARTESIAN_POINT('',(0.346410161513775,-0.8,0.));
#6362=CARTESIAN_POINT('',(0.173205080756888,-0.8,-0.3));
#6363=CARTESIAN_POINT('',(0.346410161513775,-0.8,0.));
#6364=CARTESIAN_POINT('',(0.173205080756888,-1.28,-0.3));
#6365=CARTESIAN_POINT('',(0.173205080756888,-0.8,-0.3));
#6366=CARTESIAN_POINT('',(0.346410161513775,-1.28,0.));
#6367=CARTESIAN_POINT('',(0.346410161513775,-1.28,0.));
#6368=CARTESIAN_POINT('',(0.346410161513775,-0.8,0.));
#6369=CARTESIAN_POINT('Origin',(-0.173205080756888,-0.8,-0.3));
#6370=CARTESIAN_POINT('',(-0.173205080756888,-0.8,-0.3));
#6371=CARTESIAN_POINT('',(0.173205080756888,-0.8,-0.3));
#6372=CARTESIAN_POINT('',(-0.173205080756888,-1.28,-0.3));
#6373=CARTESIAN_POINT('',(-0.173205080756888,-0.8,-0.3));
#6374=CARTESIAN_POINT('',(0.173205080756888,-1.28,-0.3));
#6375=CARTESIAN_POINT('Origin',(-0.346410161513775,-0.8,-5.55111512312578E-17));
#6376=CARTESIAN_POINT('',(-0.346410161513775,-0.8,-4.24230095489963E-17));
#6377=CARTESIAN_POINT('',(-0.173205080756888,-0.8,-0.3));
#6378=CARTESIAN_POINT('',(-0.346410161513775,-1.28,-5.55111512312578E-17));
#6379=CARTESIAN_POINT('',(-0.346410161513775,-0.8,-4.24230095489963E-17));
#6380=CARTESIAN_POINT('',(-0.173205080756888,-1.28,-0.3));
#6381=CARTESIAN_POINT('Origin',(-0.173205080756888,-0.8,0.3));
#6382=CARTESIAN_POINT('',(-0.173205080756888,-0.8,0.3));
#6383=CARTESIAN_POINT('',(-0.346410161513775,-0.8,-4.24230095489963E-17));
#6384=CARTESIAN_POINT('',(-0.173205080756888,-1.28,0.3));
#6385=CARTESIAN_POINT('',(-0.173205080756888,-0.8,0.3));
#6386=CARTESIAN_POINT('',(-0.346410161513775,-1.28,-4.24230095489963E-17));
#6387=CARTESIAN_POINT('Origin',(0.173205080756888,-0.8,0.3));
#6388=CARTESIAN_POINT('',(0.173205080756888,-0.8,0.3));
#6389=CARTESIAN_POINT('',(-0.173205080756888,-0.8,0.3));
#6390=CARTESIAN_POINT('',(0.173205080756888,-1.28,0.3));
#6391=CARTESIAN_POINT('',(0.173205080756888,-0.8,0.3));
#6392=CARTESIAN_POINT('',(-0.173205080756888,-1.28,0.3));
#6393=CARTESIAN_POINT('Origin',(0.346410161513775,-0.8,0.));
#6394=CARTESIAN_POINT('',(0.173205080756888,-0.8,0.3));
#6395=CARTESIAN_POINT('',(0.173205080756888,-1.28,0.3));
#6396=CARTESIAN_POINT('Origin',(0.,-0.8,-5.55111512312578E-17));
#6397=CARTESIAN_POINT('Origin',(0.,-1.28,-5.55111512312578E-17));
#6398=CARTESIAN_POINT('Origin',(0.,-2.9,0.));
#6399=CARTESIAN_POINT('',(-0.4,-2.9,4.89858719658941E-17));
#6400=CARTESIAN_POINT('Origin',(0.,-2.9,0.));
#6401=CARTESIAN_POINT('',(-0.3933,-2.9,4.81653586104654E-17));
#6402=CARTESIAN_POINT('Origin',(0.,-2.9,0.));
#6403=CARTESIAN_POINT('Origin',(0.,-7.5,0.));
#6404=CARTESIAN_POINT('',(-0.4,-7.5,4.89858719658941E-17));
#6405=CARTESIAN_POINT('',(-0.4,-7.5,4.89858719658941E-17));
#6406=CARTESIAN_POINT('Origin',(0.,-7.5,0.));
#6407=CARTESIAN_POINT('Origin',(0.,-7.5,0.));
#6408=CARTESIAN_POINT('Origin',(0.6,0.8,0.));
#6409=CARTESIAN_POINT('',(-0.6,0.8,-7.34788079488412E-17));
#6410=CARTESIAN_POINT('Origin',(0.,0.8,0.));
#6411=CARTESIAN_POINT('Origin',(0.,0.775,0.));
#6412=CARTESIAN_POINT('',(-0.65,0.75,-7.9602041944578E-17));
#6413=CARTESIAN_POINT('Origin',(0.,0.75,0.));
#6414=CARTESIAN_POINT('',(-0.625,0.775,-7.65404249467096E-17));
#6415=CARTESIAN_POINT('Origin',(0.,0.39,0.));
#6416=CARTESIAN_POINT('',(-0.65,0.0299999999999998,-7.9602041944578E-17));
#6417=CARTESIAN_POINT('Origin',(0.,0.0299999999999998,0.));
#6418=CARTESIAN_POINT('',(-0.65,0.39,-7.9602041944578E-17));
#6419=CARTESIAN_POINT('Origin',(0.,0.0150000000000001,0.));
#6420=CARTESIAN_POINT('',(-0.62,5.89805981832114E-17,-7.59281015471359E-17));
#6421=CARTESIAN_POINT('Origin',(0.,0.,0.));
#6422=CARTESIAN_POINT('',(-0.635,0.0150000000000001,-7.77650717458569E-17));
#6423=CARTESIAN_POINT('Origin',(0.42,0.,0.));
#6424=CARTESIAN_POINT('',(-0.42,-3.46944695195361E-18,-5.14351655641888E-17));
#6425=CARTESIAN_POINT('Origin',(0.,0.,0.));
#6426=CARTESIAN_POINT('Origin',(0.,-0.02,0.));
#6427=CARTESIAN_POINT('',(-0.3933,-0.0534000000000001,4.81653586104654E-17));
#6428=CARTESIAN_POINT('Origin',(0.,-0.0534000000000001,0.));
#6429=CARTESIAN_POINT('',(-0.41,-0.02,-5.02105187650415E-17));
#6430=CARTESIAN_POINT('Origin',(0.,-1.48,0.));
#6431=CARTESIAN_POINT('',(-0.3933,-1.48,-4.81653586104654E-17));
#7560=UNCERTAINTY_MEASURE_WITH_UNIT(LENGTH_MEASURE(0.001),#7610,
'DISTANCE_ACCURACY_VALUE',
'Maximum model space distance between geometric entities at asserted c
onnectivities');
#7579=UNCERTAINTY_MEASURE_WITH_UNIT(LENGTH_MEASURE(0.001),#7610,
'DISTANCE_ACCURACY_VALUE',
'Maximum model space distance between geometric entities at asserted c
onnectivities');
#7590=(
GEOMETRIC_REPRESENTATION_CONTEXT(3)
GLOBAL_UNCERTAINTY_ASSIGNED_CONTEXT((#7560))
GLOBAL_UNIT_ASSIGNED_CONTEXT((#7610,#7612,#7613))
REPRESENTATION_CONTEXT('','3D')
);
#7609=(
GEOMETRIC_REPRESENTATION_CONTEXT(3)
GLOBAL_UNCERTAINTY_ASSIGNED_CONTEXT((#7579))
GLOBAL_UNIT_ASSIGNED_CONTEXT((#7610,#7612,#7613))
REPRESENTATION_CONTEXT('','3D')
);
#7610=(
LENGTH_UNIT()
NAMED_UNIT(*)
SI_UNIT(.CENTI.,.METRE.)
);
#7612=(
NAMED_UNIT(*)
PLANE_ANGLE_UNIT()
SI_UNIT($,.RADIAN.)
);
#7613=(
NAMED_UNIT(*)
SI_UNIT($,.STERADIAN.)
SOLID_ANGLE_UNIT()
);
#7624=SHAPE_DEFINITION_REPRESENTATION(#7653,#7730);
#7653=PRODUCT_DEFINITION_SHAPE('',$,#7760);
#7730=SHAPE_REPRESENTATION('',(#4356),#7590);
#7749=PRODUCT_DEFINITION_CONTEXT('part definition',#7838,'design');
#7760=PRODUCT_DEFINITION('M8x75 cross bolt','M8x75 cross bolt',#7789,#7749);
#7789=PRODUCT_DEFINITION_FORMATION('',$,#7850);
#7838=APPLICATION_CONTEXT(
'Core Data for Automotive Mechanical Design Process');
#7839=PRODUCT_CONTEXT('part definition',#7838,'mechanical');
#7850=PRODUCT('M8x75 cross bolt','M8x75 cross bolt','M8x75 cross bolt',
(#7839));
#7932=COLOUR_RGB('Black',0.12,0.14,0.17);
#7933=FILL_AREA_STYLE_COLOUR('',#7932);
#7934=FILL_AREA_STYLE('',(#7933));
#7935=SURFACE_STYLE_FILL_AREA(#7934);
#7936=SURFACE_SIDE_STYLE('',(#7935));
#7937=SURFACE_STYLE_USAGE(.BOTH.,#7936);
#7938=PRESENTATION_STYLE_ASSIGNMENT((#7937));
ENDSEC;
END-ISO-10303-21;
